ISO-10303-21;
HEADER;
/* Generated by software containing ST-Developer
 * from STEP Tools, Inc. (www.steptools.com) 
 */

FILE_DESCRIPTION(
/* description */ ('Single-Axis Profile-Rail Linear Slide'),
/* implementation_level */ '2;1');

FILE_NAME(
/* name */ 'M4x10 Cap Screw.step',
/* time_stamp */ '2026-10-27T10:47:43-07:00',
/* author */ (''),
/* organization */ (''),
/* preprocessor_version */ 'ST-DEVELOPER v20.2',
/* originating_system */ 'Autodesk Translation Framework v15.17.0.0',
/* authorisation */ '');

FILE_SCHEMA (('AUTOMOTIVE_DESIGN { 1 0 10303 214 3 1 1 }'));
ENDSEC;

DATA;
#10=MECHANICAL_DESIGN_GEOMETRIC_PRESENTATION_REPRESENTATION('',(#343),#14478);
#246=CONICAL_SURFACE('',#9334,0.325,0.785398163397448);
#247=CONICAL_SURFACE('',#9338,0.335,0.785398163397448);
#248=CONICAL_SURFACE('',#9342,0.21,0.463647609000806);
#264=ORIENTED_CLOSED_SHELL('',*,#8604,.F.);
#269=BREP_WITH_VOIDS('Body1',#8605,(#264));
#289=SHAPE_REPRESENTATION_RELATIONSHIP('SRR','None',#14619,#316);
#316=ADVANCED_BREP_SHAPE_REPRESENTATION('',(#269),#14463);
#343=STYLED_ITEM('',(#14838),#269);
#438=FACE_BOUND('',#1676,.T.);
#736=PLANE('',#9322);
#737=PLANE('',#9323);
#738=PLANE('',#9324);
#739=PLANE('',#9325);
#740=PLANE('',#9326);
#741=PLANE('',#9327);
#742=PLANE('',#9328);
#743=PLANE('',#9329);
#744=PLANE('',#9330);
#745=PLANE('',#9332);
#746=PLANE('',#9340);
#1147=FACE_OUTER_BOUND('',#1662,.T.);
#1148=FACE_OUTER_BOUND('',#1663,.T.);
#1149=FACE_OUTER_BOUND('',#1664,.T.);
#1150=FACE_OUTER_BOUND('',#1665,.T.);
#1151=FACE_OUTER_BOUND('',#1666,.T.);
#1152=FACE_OUTER_BOUND('',#1667,.T.);
#1153=FACE_OUTER_BOUND('',#1668,.T.);
#1154=FACE_OUTER_BOUND('',#1669,.T.);
#1155=FACE_OUTER_BOUND('',#1670,.T.);
#1156=FACE_OUTER_BOUND('',#1671,.T.);
#1157=FACE_OUTER_BOUND('',#1672,.T.);
#1158=FACE_OUTER_BOUND('',#1673,.T.);
#1159=FACE_OUTER_BOUND('',#1674,.T.);
#1160=FACE_OUTER_BOUND('',#1675,.T.);
#1161=FACE_OUTER_BOUND('',#1677,.T.);
#1162=FACE_OUTER_BOUND('',#1678,.T.);
#1662=EDGE_LOOP('',(#7421,#7422,#7423,#7424));
#1663=EDGE_LOOP('',(#7425,#7426,#7427,#7428));
#1664=EDGE_LOOP('',(#7429,#7430,#7431,#7432));
#1665=EDGE_LOOP('',(#7433,#7434,#7435,#7436));
#1666=EDGE_LOOP('',(#7437,#7438,#7439,#7440));
#1667=EDGE_LOOP('',(#7441,#7442,#7443,#7444));
#1668=EDGE_LOOP('',(#7445,#7446,#7447,#7448,#7449,#7450));
#1669=EDGE_LOOP('',(#7451,#7452,#7453,#7454,#7455,#7456));
#1670=EDGE_LOOP('',(#7457));
#1671=EDGE_LOOP('',(#7458));
#1672=EDGE_LOOP('',(#7459,#7460,#7461,#7462));
#1673=EDGE_LOOP('',(#7463,#7464,#7465,#7466));
#1674=EDGE_LOOP('',(#7467,#7468,#7469,#7470));
#1675=EDGE_LOOP('',(#7471));
#1676=EDGE_LOOP('',(#7472));
#1677=EDGE_LOOP('',(#7473,#7474,#7475,#7476));
#1678=EDGE_LOOP('',(#7477,#7478,#7479,#7480));
#2565=LINE('',#13662,#3536);
#2566=LINE('',#13664,#3537);
#2567=LINE('',#13666,#3538);
#2568=LINE('',#13667,#3539);
#2569=LINE('',#13670,#3540);
#2570=LINE('',#13672,#3541);
#2571=LINE('',#13673,#3542);
#2572=LINE('',#13676,#3543);
#2573=LINE('',#13678,#3544);
#2574=LINE('',#13679,#3545);
#2575=LINE('',#13682,#3546);
#2576=LINE('',#13684,#3547);
#2577=LINE('',#13685,#3548);
#2578=LINE('',#13688,#3549);
#2579=LINE('',#13690,#3550);
#2580=LINE('',#13691,#3551);
#2581=LINE('',#13693,#3552);
#2582=LINE('',#13694,#3553);
#2583=LINE('',#13706,#3554);
#2584=LINE('',#13710,#3555);
#2585=LINE('',#13714,#3556);
#2586=LINE('',#13721,#3557);
#2587=LINE('',#13723,#3558);
#3536=VECTOR('',#11154,1.);
#3537=VECTOR('',#11155,1.);
#3538=VECTOR('',#11156,1.);
#3539=VECTOR('',#11157,1.);
#3540=VECTOR('',#11160,1.);
#3541=VECTOR('',#11161,1.);
#3542=VECTOR('',#11162,1.);
#3543=VECTOR('',#11165,1.);
#3544=VECTOR('',#11166,1.);
#3545=VECTOR('',#11167,1.);
#3546=VECTOR('',#11170,1.);
#3547=VECTOR('',#11171,1.);
#3548=VECTOR('',#11172,1.);
#3549=VECTOR('',#11175,1.);
#3550=VECTOR('',#11176,1.);
#3551=VECTOR('',#11177,1.);
#3552=VECTOR('',#11180,1.);
#3553=VECTOR('',#11181,1.);
#3554=VECTOR('',#11198,0.325);
#3555=VECTOR('',#11203,0.35);
#3556=VECTOR('',#11208,0.335);
#3557=VECTOR('',#11217,0.21);
#3558=VECTOR('',#11220,0.2);
#3859=CIRCLE('',#9331,0.1954);
#3860=CIRCLE('',#9333,0.3);
#3861=CIRCLE('',#9335,0.35);
#3862=CIRCLE('',#9337,0.35);
#3863=CIRCLE('',#9339,0.32);
#3864=CIRCLE('',#9341,0.22);
#3865=CIRCLE('',#9343,0.1954);
#4473=VERTEX_POINT('',#13660);
#4474=VERTEX_POINT('',#13661);
#4475=VERTEX_POINT('',#13663);
#4476=VERTEX_POINT('',#13665);
#4477=VERTEX_POINT('',#13669);
#4478=VERTEX_POINT('',#13671);
#4479=VERTEX_POINT('',#13675);
#4480=VERTEX_POINT('',#13677);
#4481=VERTEX_POINT('',#13681);
#4482=VERTEX_POINT('',#13683);
#4483=VERTEX_POINT('',#13687);
#4484=VERTEX_POINT('',#13689);
#4485=VERTEX_POINT('',#13698);
#4486=VERTEX_POINT('',#13701);
#4487=VERTEX_POINT('',#13704);
#4488=VERTEX_POINT('',#13708);
#4489=VERTEX_POINT('',#13712);
#4490=VERTEX_POINT('',#13716);
#4491=VERTEX_POINT('',#13719);
#5488=EDGE_CURVE('',#4473,#4474,#2565,.T.);
#5489=EDGE_CURVE('',#4474,#4475,#2566,.T.);
#5490=EDGE_CURVE('',#4475,#4476,#2567,.T.);
#5491=EDGE_CURVE('',#4473,#4476,#2568,.T.);
#5492=EDGE_CURVE('',#4474,#4477,#2569,.T.);
#5493=EDGE_CURVE('',#4477,#4478,#2570,.T.);
#5494=EDGE_CURVE('',#4478,#4475,#2571,.T.);
#5495=EDGE_CURVE('',#4477,#4479,#2572,.T.);
#5496=EDGE_CURVE('',#4479,#4480,#2573,.T.);
#5497=EDGE_CURVE('',#4480,#4478,#2574,.T.);
#5498=EDGE_CURVE('',#4479,#4481,#2575,.T.);
#5499=EDGE_CURVE('',#4481,#4482,#2576,.T.);
#5500=EDGE_CURVE('',#4482,#4480,#2577,.T.);
#5501=EDGE_CURVE('',#4481,#4483,#2578,.T.);
#5502=EDGE_CURVE('',#4483,#4484,#2579,.T.);
#5503=EDGE_CURVE('',#4484,#4482,#2580,.T.);
#5504=EDGE_CURVE('',#4483,#4473,#2581,.T.);
#5505=EDGE_CURVE('',#4476,#4484,#2582,.T.);
#5506=EDGE_CURVE('',#4485,#4485,#3859,.T.);
#5507=EDGE_CURVE('',#4486,#4486,#3860,.T.);
#5508=EDGE_CURVE('',#4487,#4487,#3861,.T.);
#5509=EDGE_CURVE('',#4487,#4486,#2583,.T.);
#5510=EDGE_CURVE('',#4488,#4488,#3862,.T.);
#5511=EDGE_CURVE('',#4488,#4487,#2584,.T.);
#5512=EDGE_CURVE('',#4489,#4489,#3863,.T.);
#5513=EDGE_CURVE('',#4489,#4488,#2585,.T.);
#5514=EDGE_CURVE('',#4490,#4490,#3864,.T.);
#5515=EDGE_CURVE('',#4491,#4491,#3865,.F.);
#5516=EDGE_CURVE('',#4491,#4490,#2586,.T.);
#5517=EDGE_CURVE('',#4485,#4491,#2587,.T.);
#7421=ORIENTED_EDGE('',*,*,#5488,.T.);
#7422=ORIENTED_EDGE('',*,*,#5489,.T.);
#7423=ORIENTED_EDGE('',*,*,#5490,.T.);
#7424=ORIENTED_EDGE('',*,*,#5491,.F.);
#7425=ORIENTED_EDGE('',*,*,#5492,.T.);
#7426=ORIENTED_EDGE('',*,*,#5493,.T.);
#7427=ORIENTED_EDGE('',*,*,#5494,.T.);
#7428=ORIENTED_EDGE('',*,*,#5489,.F.);
#7429=ORIENTED_EDGE('',*,*,#5495,.T.);
#7430=ORIENTED_EDGE('',*,*,#5496,.T.);
#7431=ORIENTED_EDGE('',*,*,#5497,.T.);
#7432=ORIENTED_EDGE('',*,*,#5493,.F.);
#7433=ORIENTED_EDGE('',*,*,#5498,.T.);
#7434=ORIENTED_EDGE('',*,*,#5499,.T.);
#7435=ORIENTED_EDGE('',*,*,#5500,.T.);
#7436=ORIENTED_EDGE('',*,*,#5496,.F.);
#7437=ORIENTED_EDGE('',*,*,#5501,.T.);
#7438=ORIENTED_EDGE('',*,*,#5502,.T.);
#7439=ORIENTED_EDGE('',*,*,#5503,.T.);
#7440=ORIENTED_EDGE('',*,*,#5499,.F.);
#7441=ORIENTED_EDGE('',*,*,#5504,.T.);
#7442=ORIENTED_EDGE('',*,*,#5491,.T.);
#7443=ORIENTED_EDGE('',*,*,#5505,.T.);
#7444=ORIENTED_EDGE('',*,*,#5502,.F.);
#7445=ORIENTED_EDGE('',*,*,#5504,.F.);
#7446=ORIENTED_EDGE('',*,*,#5501,.F.);
#7447=ORIENTED_EDGE('',*,*,#5498,.F.);
#7448=ORIENTED_EDGE('',*,*,#5495,.F.);
#7449=ORIENTED_EDGE('',*,*,#5492,.F.);
#7450=ORIENTED_EDGE('',*,*,#5488,.F.);
#7451=ORIENTED_EDGE('',*,*,#5505,.F.);
#7452=ORIENTED_EDGE('',*,*,#5490,.F.);
#7453=ORIENTED_EDGE('',*,*,#5494,.F.);
#7454=ORIENTED_EDGE('',*,*,#5497,.F.);
#7455=ORIENTED_EDGE('',*,*,#5500,.F.);
#7456=ORIENTED_EDGE('',*,*,#5503,.F.);
#7457=ORIENTED_EDGE('',*,*,#5506,.F.);
#7458=ORIENTED_EDGE('',*,*,#5507,.F.);
#7459=ORIENTED_EDGE('',*,*,#5508,.F.);
#7460=ORIENTED_EDGE('',*,*,#5509,.T.);
#7461=ORIENTED_EDGE('',*,*,#5507,.T.);
#7462=ORIENTED_EDGE('',*,*,#5509,.F.);
#7463=ORIENTED_EDGE('',*,*,#5510,.F.);
#7464=ORIENTED_EDGE('',*,*,#5511,.T.);
#7465=ORIENTED_EDGE('',*,*,#5508,.T.);
#7466=ORIENTED_EDGE('',*,*,#5511,.F.);
#7467=ORIENTED_EDGE('',*,*,#5512,.F.);
#7468=ORIENTED_EDGE('',*,*,#5513,.T.);
#7469=ORIENTED_EDGE('',*,*,#5510,.T.);
#7470=ORIENTED_EDGE('',*,*,#5513,.F.);
#7471=ORIENTED_EDGE('',*,*,#5512,.T.);
#7472=ORIENTED_EDGE('',*,*,#5514,.F.);
#7473=ORIENTED_EDGE('',*,*,#5515,.F.);
#7474=ORIENTED_EDGE('',*,*,#5516,.T.);
#7475=ORIENTED_EDGE('',*,*,#5514,.T.);
#7476=ORIENTED_EDGE('',*,*,#5516,.F.);
#7477=ORIENTED_EDGE('',*,*,#5506,.T.);
#7478=ORIENTED_EDGE('',*,*,#5517,.T.);
#7479=ORIENTED_EDGE('',*,*,#5515,.T.);
#7480=ORIENTED_EDGE('',*,*,#5517,.F.);
#8107=CYLINDRICAL_SURFACE('',#9336,0.35);
#8108=CYLINDRICAL_SURFACE('',#9344,0.1954);
#8441=ADVANCED_FACE('',(#1147),#736,.F.);
#8442=ADVANCED_FACE('',(#1148),#737,.F.);
#8443=ADVANCED_FACE('',(#1149),#738,.F.);
#8444=ADVANCED_FACE('',(#1150),#739,.F.);
#8445=ADVANCED_FACE('',(#1151),#740,.F.);
#8446=ADVANCED_FACE('',(#1152),#741,.F.);
#8447=ADVANCED_FACE('',(#1153),#742,.F.);
#8448=ADVANCED_FACE('',(#1154),#743,.F.);
#8449=ADVANCED_FACE('',(#1155),#744,.F.);
#8450=ADVANCED_FACE('',(#1156),#745,.T.);
#8451=ADVANCED_FACE('',(#1157),#246,.T.);
#8452=ADVANCED_FACE('',(#1158),#8107,.T.);
#8453=ADVANCED_FACE('',(#1159),#247,.T.);
#8454=ADVANCED_FACE('',(#1160,#438),#746,.T.);
#8455=ADVANCED_FACE('',(#1161),#248,.T.);
#8456=ADVANCED_FACE('',(#1162),#8108,.T.);
#8604=CLOSED_SHELL('',(#8441,#8442,#8443,#8444,#8445,#8446,#8447,#8448));
#8605=CLOSED_SHELL('',(#8449,#8450,#8451,#8452,#8453,#8454,#8455,#8456));
#9321=AXIS2_PLACEMENT_3D('',#13658,#11150,#11151);
#9322=AXIS2_PLACEMENT_3D('',#13659,#11152,#11153);
#9323=AXIS2_PLACEMENT_3D('',#13668,#11158,#11159);
#9324=AXIS2_PLACEMENT_3D('',#13674,#11163,#11164);
#9325=AXIS2_PLACEMENT_3D('',#13680,#11168,#11169);
#9326=AXIS2_PLACEMENT_3D('',#13686,#11173,#11174);
#9327=AXIS2_PLACEMENT_3D('',#13692,#11178,#11179);
#9328=AXIS2_PLACEMENT_3D('',#13695,#11182,#11183);
#9329=AXIS2_PLACEMENT_3D('',#13696,#11184,#11185);
#9330=AXIS2_PLACEMENT_3D('',#13697,#11186,#11187);
#9331=AXIS2_PLACEMENT_3D('',#13699,#11188,#11189);
#9332=AXIS2_PLACEMENT_3D('',#13700,#11190,#11191);
#9333=AXIS2_PLACEMENT_3D('',#13702,#11192,#11193);
#9334=AXIS2_PLACEMENT_3D('',#13703,#11194,#11195);
#9335=AXIS2_PLACEMENT_3D('',#13705,#11196,#11197);
#9336=AXIS2_PLACEMENT_3D('',#13707,#11199,#11200);
#9337=AXIS2_PLACEMENT_3D('',#13709,#11201,#11202);
#9338=AXIS2_PLACEMENT_3D('',#13711,#11204,#11205);
#9339=AXIS2_PLACEMENT_3D('',#13713,#11206,#11207);
#9340=AXIS2_PLACEMENT_3D('',#13715,#11209,#11210);
#9341=AXIS2_PLACEMENT_3D('',#13717,#11211,#11212);
#9342=AXIS2_PLACEMENT_3D('',#13718,#11213,#11214);
#9343=AXIS2_PLACEMENT_3D('',#13720,#11215,#11216);
#9344=AXIS2_PLACEMENT_3D('',#13722,#11218,#11219);
#11150=DIRECTION('axis',(0.,0.,1.));
#11151=DIRECTION('refdir',(1.,0.,0.));
#11152=DIRECTION('center_axis',(0.866025403784439,0.,-0.5));
#11153=DIRECTION('ref_axis',(0.5,0.,0.866025403784439));
#11154=DIRECTION('',(-0.5,0.,-0.866025403784439));
#11155=DIRECTION('',(0.,-1.,0.));
#11156=DIRECTION('',(0.5,0.,0.866025403784439));
#11157=DIRECTION('',(0.,-1.,0.));
#11158=DIRECTION('center_axis',(1.60246890531964E-16,0.,-1.));
#11159=DIRECTION('ref_axis',(1.,0.,1.60246890531964E-16));
#11160=DIRECTION('',(-1.,0.,-1.60246890531964E-16));
#11161=DIRECTION('',(0.,-1.,0.));
#11162=DIRECTION('',(1.,0.,1.60246890531964E-16));
#11163=DIRECTION('center_axis',(-0.866025403784439,0.,-0.5));
#11164=DIRECTION('ref_axis',(0.5,0.,-0.866025403784439));
#11165=DIRECTION('',(-0.5,0.,0.866025403784439));
#11166=DIRECTION('',(0.,-1.,0.));
#11167=DIRECTION('',(0.5,0.,-0.866025403784439));
#11168=DIRECTION('center_axis',(-0.866025403784439,0.,0.5));
#11169=DIRECTION('ref_axis',(-0.5,0.,-0.866025403784439));
#11170=DIRECTION('',(0.5,0.,0.866025403784439));
#11171=DIRECTION('',(0.,-1.,0.));
#11172=DIRECTION('',(-0.5,0.,-0.866025403784439));
#11173=DIRECTION('center_axis',(-1.60246890531964E-16,0.,1.));
#11174=DIRECTION('ref_axis',(-1.,0.,-1.60246890531964E-16));
#11175=DIRECTION('',(1.,0.,1.60246890531964E-16));
#11176=DIRECTION('',(0.,-1.,0.));
#11177=DIRECTION('',(-1.,0.,-1.60246890531964E-16));
#11178=DIRECTION('center_axis',(0.866025403784439,0.,0.5));
#11179=DIRECTION('ref_axis',(-0.5,0.,0.866025403784439));
#11180=DIRECTION('',(0.5,0.,-0.866025403784439));
#11181=DIRECTION('',(-0.5,0.,0.866025403784439));
#11182=DIRECTION('center_axis',(0.,1.,0.));
#11183=DIRECTION('ref_axis',(1.,0.,0.));
#11184=DIRECTION('center_axis',(0.,-1.,0.));
#11185=DIRECTION('ref_axis',(0.,0.,-1.));
#11186=DIRECTION('center_axis',(0.,1.,0.));
#11187=DIRECTION('ref_axis',(1.,0.,0.));
#11188=DIRECTION('center_axis',(0.,1.,0.));
#11189=DIRECTION('ref_axis',(1.,0.,0.));
#11190=DIRECTION('center_axis',(0.,1.,0.));
#11191=DIRECTION('ref_axis',(0.,0.,1.));
#11192=DIRECTION('center_axis',(0.,-1.,0.));
#11193=DIRECTION('ref_axis',(1.,0.,0.));
#11194=DIRECTION('center_axis',(0.,-1.,0.));
#11195=DIRECTION('ref_axis',(1.,0.,0.));
#11196=DIRECTION('center_axis',(0.,-1.,0.));
#11197=DIRECTION('ref_axis',(1.,0.,0.));
#11198=DIRECTION('',(0.707106781186547,0.707106781186548,8.65956056235493E-17));
#11199=DIRECTION('center_axis',(0.,-1.,0.));
#11200=DIRECTION('ref_axis',(1.,0.,0.));
#11201=DIRECTION('center_axis',(0.,-1.,0.));
#11202=DIRECTION('ref_axis',(1.,0.,0.));
#11203=DIRECTION('',(0.,1.,0.));
#11204=DIRECTION('center_axis',(0.,1.,0.));
#11205=DIRECTION('ref_axis',(1.,0.,0.));
#11206=DIRECTION('center_axis',(0.,-1.,0.));
#11207=DIRECTION('ref_axis',(1.,0.,0.));
#11208=DIRECTION('',(-0.707106781186547,0.707106781186548,-8.65956056235493E-17));
#11209=DIRECTION('center_axis',(0.,-1.,0.));
#11210=DIRECTION('ref_axis',(0.,0.,-1.));
#11211=DIRECTION('center_axis',(0.,-1.,0.));
#11212=DIRECTION('ref_axis',(1.,0.,0.));
#11213=DIRECTION('center_axis',(0.,1.,0.));
#11214=DIRECTION('ref_axis',(1.,0.,0.));
#11215=DIRECTION('center_axis',(0.,1.,0.));
#11216=DIRECTION('ref_axis',(1.,0.,0.));
#11217=DIRECTION('',(-0.447213595499958,0.894427190999916,-5.47678698264203E-17));
#11218=DIRECTION('center_axis',(0.,-1.,0.));
#11219=DIRECTION('ref_axis',(1.,0.,0.));
#11220=DIRECTION('',(0.,1.,0.));
#13658=CARTESIAN_POINT('',(0.,0.,0.));
#13659=CARTESIAN_POINT('Origin',(0.0866025403784439,-0.4,-0.15));
#13660=CARTESIAN_POINT('',(0.173205080756888,-0.4,0.));
#13661=CARTESIAN_POINT('',(0.0866025403784439,-0.4,-0.15));
#13662=CARTESIAN_POINT('',(0.173205080756888,-0.4,0.));
#13663=CARTESIAN_POINT('',(0.0866025403784439,-0.64,-0.15));
#13664=CARTESIAN_POINT('',(0.0866025403784439,-0.4,-0.15));
#13665=CARTESIAN_POINT('',(0.173205080756888,-0.64,0.));
#13666=CARTESIAN_POINT('',(0.173205080756888,-0.64,0.));
#13667=CARTESIAN_POINT('',(0.173205080756888,-0.4,0.));
#13668=CARTESIAN_POINT('Origin',(-0.0866025403784438,-0.4,-0.15));
#13669=CARTESIAN_POINT('',(-0.0866025403784438,-0.4,-0.15));
#13670=CARTESIAN_POINT('',(0.0866025403784439,-0.4,-0.15));
#13671=CARTESIAN_POINT('',(-0.0866025403784438,-0.64,-0.15));
#13672=CARTESIAN_POINT('',(-0.0866025403784438,-0.4,-0.15));
#13673=CARTESIAN_POINT('',(0.0866025403784439,-0.64,-0.15));
#13674=CARTESIAN_POINT('Origin',(-0.173205080756888,-0.4,-2.77555756156289E-17));
#13675=CARTESIAN_POINT('',(-0.173205080756888,-0.4,-2.12115047744981E-17));
#13676=CARTESIAN_POINT('',(-0.0866025403784438,-0.4,-0.15));
#13677=CARTESIAN_POINT('',(-0.173205080756888,-0.64,-2.77555756156289E-17));
#13678=CARTESIAN_POINT('',(-0.173205080756888,-0.4,-2.12115047744981E-17));
#13679=CARTESIAN_POINT('',(-0.0866025403784438,-0.64,-0.15));
#13680=CARTESIAN_POINT('Origin',(-0.0866025403784439,-0.4,0.15));
#13681=CARTESIAN_POINT('',(-0.0866025403784439,-0.4,0.15));
#13682=CARTESIAN_POINT('',(-0.173205080756888,-0.4,-2.12115047744981E-17));
#13683=CARTESIAN_POINT('',(-0.0866025403784439,-0.64,0.15));
#13684=CARTESIAN_POINT('',(-0.0866025403784439,-0.4,0.15));
#13685=CARTESIAN_POINT('',(-0.173205080756888,-0.64,-2.12115047744981E-17));
#13686=CARTESIAN_POINT('Origin',(0.0866025403784439,-0.4,0.15));
#13687=CARTESIAN_POINT('',(0.0866025403784439,-0.4,0.15));
#13688=CARTESIAN_POINT('',(-0.0866025403784439,-0.4,0.15));
#13689=CARTESIAN_POINT('',(0.0866025403784439,-0.64,0.15));
#13690=CARTESIAN_POINT('',(0.0866025403784439,-0.4,0.15));
#13691=CARTESIAN_POINT('',(-0.0866025403784439,-0.64,0.15));
#13692=CARTESIAN_POINT('Origin',(0.173205080756888,-0.4,0.));
#13693=CARTESIAN_POINT('',(0.0866025403784439,-0.4,0.15));
#13694=CARTESIAN_POINT('',(0.0866025403784439,-0.64,0.15));
#13695=CARTESIAN_POINT('Origin',(0.,-0.4,-2.77555756156289E-17));
#13696=CARTESIAN_POINT('Origin',(0.,-0.64,-2.77555756156289E-17));
#13697=CARTESIAN_POINT('Origin',(0.,-1.,0.));
#13698=CARTESIAN_POINT('',(-0.1954,-1.,2.39295984553393E-17));
#13699=CARTESIAN_POINT('Origin',(0.,-1.,0.));
#13700=CARTESIAN_POINT('Origin',(0.3,0.4,0.));
#13701=CARTESIAN_POINT('',(-0.3,0.4,-3.67394039744206E-17));
#13702=CARTESIAN_POINT('Origin',(0.,0.4,0.));
#13703=CARTESIAN_POINT('Origin',(0.,0.375,0.));
#13704=CARTESIAN_POINT('',(-0.35,0.35,-4.28626379701573E-17));
#13705=CARTESIAN_POINT('Origin',(0.,0.35,0.));
#13706=CARTESIAN_POINT('',(-0.325,0.375,-3.9801020972289E-17));
#13707=CARTESIAN_POINT('Origin',(0.,0.19,0.));
#13708=CARTESIAN_POINT('',(-0.35,0.03,-4.28626379701574E-17));
#13709=CARTESIAN_POINT('Origin',(0.,0.03,0.));
#13710=CARTESIAN_POINT('',(-0.35,0.19,-4.28626379701574E-17));
#13711=CARTESIAN_POINT('Origin',(0.,0.0149999999999999,0.));
#13712=CARTESIAN_POINT('',(-0.32,-3.29597460435593E-17,-3.91886975727153E-17));
#13713=CARTESIAN_POINT('Origin',(0.,0.,0.));
#13714=CARTESIAN_POINT('',(-0.335,0.0149999999999999,-4.10256677714363E-17));
#13715=CARTESIAN_POINT('Origin',(0.22,0.,0.));
#13716=CARTESIAN_POINT('',(-0.22,-6.93889390390723E-18,-2.69422295812418E-17));
#13717=CARTESIAN_POINT('Origin',(0.,0.,0.));
#13718=CARTESIAN_POINT('Origin',(0.,-0.02,0.));
#13719=CARTESIAN_POINT('',(-0.1954,-0.0492,2.39295984553393E-17));
#13720=CARTESIAN_POINT('Origin',(0.,-0.0492,0.));
#13721=CARTESIAN_POINT('',(-0.21,-0.02,-2.57175827820944E-17));
#13722=CARTESIAN_POINT('Origin',(0.,-0.8,0.));
#13723=CARTESIAN_POINT('',(-0.1954,-0.8,-2.39295984553393E-17));
#14431=UNCERTAINTY_MEASURE_WITH_UNIT(LENGTH_MEASURE(0.001),#14479,
'DISTANCE_ACCURACY_VALUE',
'Maximum model space distance between geometric entities at asserted c
onnectivities');
#14446=UNCERTAINTY_MEASURE_WITH_UNIT(LENGTH_MEASURE(0.001),#14479,
'DISTANCE_ACCURACY_VALUE',
'Maximum model space distance between geometric entities at asserted c
onnectivities');
#14463=(
GEOMETRIC_REPRESENTATION_CONTEXT(3)
GLOBAL_UNCERTAINTY_ASSIGNED_CONTEXT((#14431))
GLOBAL_UNIT_ASSIGNED_CONTEXT((#14479,#14481,#14482))
REPRESENTATION_CONTEXT('','3D')
);
#14478=(
GEOMETRIC_REPRESENTATION_CONTEXT(3)
GLOBAL_UNCERTAINTY_ASSIGNED_CONTEXT((#14446))
GLOBAL_UNIT_ASSIGNED_CONTEXT((#14479,#14481,#14482))
REPRESENTATION_CONTEXT('','3D')
);
#14479=(
LENGTH_UNIT()
NAMED_UNIT(*)
SI_UNIT(.CENTI.,.METRE.)
);
#14481=(
NAMED_UNIT(*)
PLANE_ANGLE_UNIT()
SI_UNIT($,.RADIAN.)
);
#14482=(
NAMED_UNIT(*)
SI_UNIT($,.STERADIAN.)
SOLID_ANGLE_UNIT()
);
#14499=SHAPE_DEFINITION_REPRESENTATION(#14530,#14619);
#14530=PRODUCT_DEFINITION_SHAPE('',$,#14651);
#14619=SHAPE_REPRESENTATION('',(#9321),#14463);
#14634=PRODUCT_DEFINITION_CONTEXT('part definition',#14729,'design');
#14651=PRODUCT_DEFINITION('M4x10 Cap Screw','M4x10 Cap Screw',#14682,#14634);
#14682=PRODUCT_DEFINITION_FORMATION('',$,#14747);
#14729=APPLICATION_CONTEXT(
'Core Data for Automotive Mechanical Design Process');
#14730=PRODUCT_CONTEXT('part definition',#14729,'mechanical');
#14747=PRODUCT('M4x10 Cap Screw','M4x10 Cap Screw','M4x10 Cap Screw',(#14730));
#14832=COLOUR_RGB('Black',0.12,0.14,0.17);
#14833=FILL_AREA_STYLE_COLOUR('',#14832);
#14834=FILL_AREA_STYLE('',(#14833));
#14835=SURFACE_STYLE_FILL_AREA(#14834);
#14836=SURFACE_SIDE_STYLE('',(#14835));
#14837=SURFACE_STYLE_USAGE(.BOTH.,#14836);
#14838=PRESENTATION_STYLE_ASSIGNMENT((#14837));
ENDSEC;
END-ISO-10303-21;
